ISO-10303-21;
HEADER;
/* Generated by software containing ST-Developer
 * from STEP Tools, Inc. (www.steptools.com) 
 */

FILE_DESCRIPTION(
/* description */ ('Cylinder foot and clevis mount kit'),
/* implementation_level */ '2;1');

FILE_NAME(
/* name */ 'Flat Washer - M6.step',
/* time_stamp */ '2026-10-27T20:10:43-07:00',
/* author */ (''),
/* organization */ (''),
/* preprocessor_version */ 'ST-DEVELOPER v20.2',
/* originating_system */ 'Autodesk Translation Framework v15.17.0.0',
/* authorisation */ '');

FILE_SCHEMA (('AUTOMOTIVE_DESIGN { 1 0 10303 214 3 1 1 }'));
ENDSEC;

DATA;
#10=MECHANICAL_DESIGN_GEOMETRIC_PRESENTATION_REPRESENTATION('',(#364),#9102);
#308=SHAPE_REPRESENTATION_RELATIONSHIP('SRR','None',#9257,#336);
#336=ADVANCED_BREP_SHAPE_REPRESENTATION('',(#390),#9100);
#364=STYLED_ITEM('',(#9467),#390);
#390=MANIFOLD_SOLID_BREP('Body1',#4952);
#492=FACE_BOUND('',#1401,.T.);
#493=FACE_BOUND('',#1403,.T.);
#690=PLANE('',#5865);
#691=PLANE('',#5866);
#992=FACE_OUTER_BOUND('',#1398,.T.);
#993=FACE_OUTER_BOUND('',#1399,.T.);
#994=FACE_OUTER_BOUND('',#1400,.T.);
#995=FACE_OUTER_BOUND('',#1402,.T.);
#1398=EDGE_LOOP('',(#4485,#4486,#4487,#4488));
#1399=EDGE_LOOP('',(#4489,#4490,#4491,#4492));
#1400=EDGE_LOOP('',(#4493));
#1401=EDGE_LOOP('',(#4494));
#1402=EDGE_LOOP('',(#4495));
#1403=EDGE_LOOP('',(#4496));
#1752=LINE('',#8938,#2101);
#1753=LINE('',#8944,#2102);
#2101=VECTOR('',#7429,0.32);
#2102=VECTOR('',#7436,0.6);
#2319=CIRCLE('',#5860,0.32);
#2320=CIRCLE('',#5861,0.32);
#2321=CIRCLE('',#5863,0.6);
#2322=CIRCLE('',#5864,0.6);
#2700=VERTEX_POINT('',#8935);
#2701=VERTEX_POINT('',#8937);
#2702=VERTEX_POINT('',#8941);
#2703=VERTEX_POINT('',#8943);
#3297=EDGE_CURVE('',#2700,#2700,#2319,.T.);
#3298=EDGE_CURVE('',#2700,#2701,#1752,.T.);
#3299=EDGE_CURVE('',#2701,#2701,#2320,.T.);
#3300=EDGE_CURVE('',#2702,#2702,#2321,.T.);
#3301=EDGE_CURVE('',#2702,#2703,#1753,.T.);
#3302=EDGE_CURVE('',#2703,#2703,#2322,.T.);
#4485=ORIENTED_EDGE('',*,*,#3297,.F.);
#4486=ORIENTED_EDGE('',*,*,#3298,.T.);
#4487=ORIENTED_EDGE('',*,*,#3299,.T.);
#4488=ORIENTED_EDGE('',*,*,#3298,.F.);
#4489=ORIENTED_EDGE('',*,*,#3300,.F.);
#4490=ORIENTED_EDGE('',*,*,#3301,.T.);
#4491=ORIENTED_EDGE('',*,*,#3302,.T.);
#4492=ORIENTED_EDGE('',*,*,#3301,.F.);
#4493=ORIENTED_EDGE('',*,*,#3300,.T.);
#4494=ORIENTED_EDGE('',*,*,#3297,.T.);
#4495=ORIENTED_EDGE('',*,*,#3302,.F.);
#4496=ORIENTED_EDGE('',*,*,#3299,.F.);
#4615=CYLINDRICAL_SURFACE('',#5859,0.32);
#4616=CYLINDRICAL_SURFACE('',#5862,0.6);
#4915=ADVANCED_FACE('',(#992),#4615,.F.);
#4916=ADVANCED_FACE('',(#993),#4616,.T.);
#4917=ADVANCED_FACE('',(#994,#492),#690,.T.);
#4918=ADVANCED_FACE('',(#995,#493),#691,.F.);
#4952=CLOSED_SHELL('',(#4915,#4916,#4917,#4918));
#5858=AXIS2_PLACEMENT_3D('',#8933,#7423,#7424);
#5859=AXIS2_PLACEMENT_3D('',#8934,#7425,#7426);
#5860=AXIS2_PLACEMENT_3D('',#8936,#7427,#7428);
#5861=AXIS2_PLACEMENT_3D('',#8939,#7430,#7431);
#5862=AXIS2_PLACEMENT_3D('',#8940,#7432,#7433);
#5863=AXIS2_PLACEMENT_3D('',#8942,#7434,#7435);
#5864=AXIS2_PLACEMENT_3D('',#8945,#7437,#7438);
#5865=AXIS2_PLACEMENT_3D('',#8946,#7439,#7440);
#5866=AXIS2_PLACEMENT_3D('',#8947,#7441,#7442);
#7423=DIRECTION('axis',(0.,0.,1.));
#7424=DIRECTION('refdir',(1.,0.,0.));
#7425=DIRECTION('center_axis',(0.,1.,0.));
#7426=DIRECTION('ref_axis',(1.,0.,0.));
#7427=DIRECTION('center_axis',(0.,-1.,0.));
#7428=DIRECTION('ref_axis',(1.,0.,0.));
#7429=DIRECTION('',(0.,-1.,0.));
#7430=DIRECTION('center_axis',(0.,-1.,0.));
#7431=DIRECTION('ref_axis',(1.,0.,0.));
#7432=DIRECTION('center_axis',(0.,1.,0.));
#7433=DIRECTION('ref_axis',(1.,0.,0.));
#7434=DIRECTION('center_axis',(0.,1.,0.));
#7435=DIRECTION('ref_axis',(1.,0.,0.));
#7436=DIRECTION('',(0.,-1.,0.));
#7437=DIRECTION('center_axis',(0.,1.,0.));
#7438=DIRECTION('ref_axis',(1.,0.,0.));
#7439=DIRECTION('center_axis',(0.,1.,0.));
#7440=DIRECTION('ref_axis',(1.,0.,0.));
#7441=DIRECTION('center_axis',(0.,1.,0.));
#7442=DIRECTION('ref_axis',(1.,0.,0.));
#8933=CARTESIAN_POINT('',(0.,0.,0.));
#8934=CARTESIAN_POINT('Origin',(0.,0.,0.));
#8935=CARTESIAN_POINT('',(-0.32,0.16,3.91886975727153E-17));
#8936=CARTESIAN_POINT('Origin',(0.,0.16,0.));
#8937=CARTESIAN_POINT('',(-0.32,0.,3.91886975727153E-17));
#8938=CARTESIAN_POINT('',(-0.32,0.,3.91886975727153E-17));
#8939=CARTESIAN_POINT('Origin',(0.,0.,0.));
#8940=CARTESIAN_POINT('Origin',(0.,0.,0.));
#8941=CARTESIAN_POINT('',(-0.6,0.16,7.34788079488412E-17));
#8942=CARTESIAN_POINT('Origin',(0.,0.16,0.));
#8943=CARTESIAN_POINT('',(-0.6,0.,7.34788079488412E-17));
#8944=CARTESIAN_POINT('',(-0.6,0.,7.34788079488412E-17));
#8945=CARTESIAN_POINT('Origin',(0.,0.,0.));
#8946=CARTESIAN_POINT('Origin',(0.,0.16,0.));
#8947=CARTESIAN_POINT('Origin',(0.,0.,0.));
#9067=UNCERTAINTY_MEASURE_WITH_UNIT(LENGTH_MEASURE(0.001),#9103,
'DISTANCE_ACCURACY_VALUE',
'Maximum model space distance between geometric entities at asserted c
onnectivities');
#9069=UNCERTAINTY_MEASURE_WITH_UNIT(LENGTH_MEASURE(0.001),#9103,
'DISTANCE_ACCURACY_VALUE',
'Maximum model space distance between geometric entities at asserted c
onnectivities');
#9100=(
GEOMETRIC_REPRESENTATION_CONTEXT(3)
GLOBAL_UNCERTAINTY_ASSIGNED_CONTEXT((#9067))
GLOBAL_UNIT_ASSIGNED_CONTEXT((#9103,#9105,#9106))
REPRESENTATION_CONTEXT('','3D')
);
#9102=(
GEOMETRIC_REPRESENTATION_CONTEXT(3)
GLOBAL_UNCERTAINTY_ASSIGNED_CONTEXT((#9069))
GLOBAL_UNIT_ASSIGNED_CONTEXT((#9103,#9105,#9106))
REPRESENTATION_CONTEXT('','3D')
);
#9103=(
LENGTH_UNIT()
NAMED_UNIT(*)
SI_UNIT(.CENTI.,.METRE.)
);
#9105=(
NAMED_UNIT(*)
PLANE_ANGLE_UNIT()
SI_UNIT($,.RADIAN.)
);
#9106=(
NAMED_UNIT(*)
SI_UNIT($,.STERADIAN.)
SOLID_ANGLE_UNIT()
);
#9137=SHAPE_DEFINITION_REPRESENTATION(#9212,#9257);
#9212=PRODUCT_DEFINITION_SHAPE('',$,#9290);
#9257=SHAPE_REPRESENTATION('',(#5858),#9100);
#9259=PRODUCT_DEFINITION_CONTEXT('part definition',#9357,'design');
#9290=PRODUCT_DEFINITION('Flat Washer - M6','Flat Washer - M6',#9322,#9259);
#9322=PRODUCT_DEFINITION_FORMATION('',$,#9389);
#9357=APPLICATION_CONTEXT(
'Core Data for Automotive Mechanical Design Process');
#9358=PRODUCT_CONTEXT('part definition',#9357,'mechanical');
#9389=PRODUCT('Flat Washer - M6','Flat Washer - M6','Flat Washer - M6',
(#9358));
#9461=COLOUR_RGB('Black',0.12,0.14,0.17);
#9462=FILL_AREA_STYLE_COLOUR('',#9461);
#9463=FILL_AREA_STYLE('',(#9462));
#9464=SURFACE_STYLE_FILL_AREA(#9463);
#9465=SURFACE_SIDE_STYLE('',(#9464));
#9466=SURFACE_STYLE_USAGE(.BOTH.,#9465);
#9467=PRESENTATION_STYLE_ASSIGNMENT((#9466));
ENDSEC;
END-ISO-10303-21;
